ISO-10303-21;
HEADER;
/* Generated by software containing ST-Developer
 * from STEP Tools, Inc. (www.steptools.com) 
 */

FILE_DESCRIPTION(
/* description */ ('Hinged panel with latch'),
/* implementation_level */ '2;1');

FILE_NAME(
/* name */ 'Flat Washer - M6.step',
/* time_stamp */ '2026-10-27T20:36:01-07:00',
/* author */ (''),
/* organization */ (''),
/* preprocessor_version */ 'ST-DEVELOPER v20.2',
/* originating_system */ 'Autodesk Translation Framework v15.17.0.0',
/* authorisation */ '');

FILE_SCHEMA (('AUTOMOTIVE_DESIGN { 1 0 10303 214 3 1 1 }'));
ENDSEC;

DATA;
#10=MECHANICAL_DESIGN_GEOMETRIC_PRESENTATION_REPRESENTATION('',(#300),#6743);
#268=SHAPE_REPRESENTATION_RELATIONSHIP('SRR','None',#6843,#284);
#284=ADVANCED_BREP_SHAPE_REPRESENTATION('',(#316),#6729);
#300=STYLED_ITEM('',(#7010),#316);
#316=MANIFOLD_SOLID_BREP('Body1',#3802);
#341=FACE_BOUND('',#827,.T.);
#342=FACE_BOUND('',#829,.T.);
#437=PLANE('',#4110);
#438=PLANE('',#4111);
#602=FACE_OUTER_BOUND('',#824,.T.);
#603=FACE_OUTER_BOUND('',#825,.T.);
#604=FACE_OUTER_BOUND('',#826,.T.);
#605=FACE_OUTER_BOUND('',#828,.T.);
#824=EDGE_LOOP('',(#3012,#3013,#3014,#3015));
#825=EDGE_LOOP('',(#3016,#3017,#3018,#3019));
#826=EDGE_LOOP('',(#3020));
#827=EDGE_LOOP('',(#3021));
#828=EDGE_LOOP('',(#3022));
#829=EDGE_LOOP('',(#3023));
#1165=LINE('',#5971,#1523);
#1166=LINE('',#5977,#1524);
#1523=VECTOR('',#4771,0.32);
#1524=VECTOR('',#4778,0.6);
#1722=CIRCLE('',#4105,0.32);
#1723=CIRCLE('',#4106,0.32);
#1724=CIRCLE('',#4108,0.6);
#1725=CIRCLE('',#4109,0.6);
#1931=VERTEX_POINT('',#5968);
#1932=VERTEX_POINT('',#5970);
#1933=VERTEX_POINT('',#5974);
#1934=VERTEX_POINT('',#5976);
#2318=EDGE_CURVE('',#1931,#1931,#1722,.T.);
#2319=EDGE_CURVE('',#1931,#1932,#1165,.T.);
#2320=EDGE_CURVE('',#1932,#1932,#1723,.T.);
#2321=EDGE_CURVE('',#1933,#1933,#1724,.T.);
#2322=EDGE_CURVE('',#1933,#1934,#1166,.T.);
#2323=EDGE_CURVE('',#1934,#1934,#1725,.T.);
#3012=ORIENTED_EDGE('',*,*,#2318,.F.);
#3013=ORIENTED_EDGE('',*,*,#2319,.T.);
#3014=ORIENTED_EDGE('',*,*,#2320,.T.);
#3015=ORIENTED_EDGE('',*,*,#2319,.F.);
#3016=ORIENTED_EDGE('',*,*,#2321,.F.);
#3017=ORIENTED_EDGE('',*,*,#2322,.T.);
#3018=ORIENTED_EDGE('',*,*,#2323,.T.);
#3019=ORIENTED_EDGE('',*,*,#2322,.F.);
#3020=ORIENTED_EDGE('',*,*,#2321,.T.);
#3021=ORIENTED_EDGE('',*,*,#2318,.T.);
#3022=ORIENTED_EDGE('',*,*,#2323,.F.);
#3023=ORIENTED_EDGE('',*,*,#2320,.F.);
#3568=CYLINDRICAL_SURFACE('',#4104,0.32);
#3569=CYLINDRICAL_SURFACE('',#4107,0.6);
#3671=ADVANCED_FACE('',(#602),#3568,.F.);
#3672=ADVANCED_FACE('',(#603),#3569,.T.);
#3673=ADVANCED_FACE('',(#604,#341),#437,.T.);
#3674=ADVANCED_FACE('',(#605,#342),#438,.F.);
#3802=CLOSED_SHELL('',(#3671,#3672,#3673,#3674));
#4103=AXIS2_PLACEMENT_3D('',#5966,#4765,#4766);
#4104=AXIS2_PLACEMENT_3D('',#5967,#4767,#4768);
#4105=AXIS2_PLACEMENT_3D('',#5969,#4769,#4770);
#4106=AXIS2_PLACEMENT_3D('',#5972,#4772,#4773);
#4107=AXIS2_PLACEMENT_3D('',#5973,#4774,#4775);
#4108=AXIS2_PLACEMENT_3D('',#5975,#4776,#4777);
#4109=AXIS2_PLACEMENT_3D('',#5978,#4779,#4780);
#4110=AXIS2_PLACEMENT_3D('',#5979,#4781,#4782);
#4111=AXIS2_PLACEMENT_3D('',#5980,#4783,#4784);
#4765=DIRECTION('axis',(0.,0.,1.));
#4766=DIRECTION('refdir',(1.,0.,0.));
#4767=DIRECTION('center_axis',(0.,1.,0.));
#4768=DIRECTION('ref_axis',(1.,0.,0.));
#4769=DIRECTION('center_axis',(0.,-1.,0.));
#4770=DIRECTION('ref_axis',(1.,0.,0.));
#4771=DIRECTION('',(0.,-1.,0.));
#4772=DIRECTION('center_axis',(0.,-1.,0.));
#4773=DIRECTION('ref_axis',(1.,0.,0.));
#4774=DIRECTION('center_axis',(0.,1.,0.));
#4775=DIRECTION('ref_axis',(1.,0.,0.));
#4776=DIRECTION('center_axis',(0.,1.,0.));
#4777=DIRECTION('ref_axis',(1.,0.,0.));
#4778=DIRECTION('',(0.,-1.,0.));
#4779=DIRECTION('center_axis',(0.,1.,0.));
#4780=DIRECTION('ref_axis',(1.,0.,0.));
#4781=DIRECTION('center_axis',(0.,1.,0.));
#4782=DIRECTION('ref_axis',(1.,0.,0.));
#4783=DIRECTION('center_axis',(0.,1.,0.));
#4784=DIRECTION('ref_axis',(1.,0.,0.));
#5966=CARTESIAN_POINT('',(0.,0.,0.));
#5967=CARTESIAN_POINT('Origin',(0.,0.,0.));
#5968=CARTESIAN_POINT('',(-0.32,0.16,3.91886975727153E-17));
#5969=CARTESIAN_POINT('Origin',(0.,0.16,0.));
#5970=CARTESIAN_POINT('',(-0.32,0.,3.91886975727153E-17));
#5971=CARTESIAN_POINT('',(-0.32,0.,3.91886975727153E-17));
#5972=CARTESIAN_POINT('Origin',(0.,0.,0.));
#5973=CARTESIAN_POINT('Origin',(0.,0.,0.));
#5974=CARTESIAN_POINT('',(-0.6,0.16,7.34788079488412E-17));
#5975=CARTESIAN_POINT('Origin',(0.,0.16,0.));
#5976=CARTESIAN_POINT('',(-0.6,0.,7.34788079488412E-17));
#5977=CARTESIAN_POINT('',(-0.6,0.,7.34788079488412E-17));
#5978=CARTESIAN_POINT('Origin',(0.,0.,0.));
#5979=CARTESIAN_POINT('Origin',(0.,0.16,0.));
#5980=CARTESIAN_POINT('Origin',(0.,0.,0.));
#6708=UNCERTAINTY_MEASURE_WITH_UNIT(LENGTH_MEASURE(0.001),#6744,
'DISTANCE_ACCURACY_VALUE',
'Maximum model space distance between geometric entities at asserted c
onnectivities');
#6722=UNCERTAINTY_MEASURE_WITH_UNIT(LENGTH_MEASURE(0.001),#6744,
'DISTANCE_ACCURACY_VALUE',
'Maximum model space distance between geometric entities at asserted c
onnectivities');
#6729=(
GEOMETRIC_REPRESENTATION_CONTEXT(3)
GLOBAL_UNCERTAINTY_ASSIGNED_CONTEXT((#6708))
GLOBAL_UNIT_ASSIGNED_CONTEXT((#6744,#6746,#6747))
REPRESENTATION_CONTEXT('','3D')
);
#6743=(
GEOMETRIC_REPRESENTATION_CONTEXT(3)
GLOBAL_UNCERTAINTY_ASSIGNED_CONTEXT((#6722))
GLOBAL_UNIT_ASSIGNED_CONTEXT((#6744,#6746,#6747))
REPRESENTATION_CONTEXT('','3D')
);
#6744=(
LENGTH_UNIT()
NAMED_UNIT(*)
SI_UNIT(.CENTI.,.METRE.)
);
#6746=(
NAMED_UNIT(*)
PLANE_ANGLE_UNIT()
SI_UNIT($,.RADIAN.)
);
#6747=(
NAMED_UNIT(*)
SI_UNIT($,.STERADIAN.)
SOLID_ANGLE_UNIT()
);
#6754=SHAPE_DEFINITION_REPRESENTATION(#6774,#6843);
#6774=PRODUCT_DEFINITION_SHAPE('',$,#6864);
#6843=SHAPE_REPRESENTATION('',(#4103),#6729);
#6857=PRODUCT_DEFINITION_CONTEXT('part definition',#6919,'design');
#6864=PRODUCT_DEFINITION('Flat Washer - M6','Flat Washer - M6',#6884,#6857);
#6884=PRODUCT_DEFINITION_FORMATION('',$,#6927);
#6919=APPLICATION_CONTEXT(
'Core Data for Automotive Mechanical Design Process');
#6920=PRODUCT_CONTEXT('part definition',#6919,'mechanical');
#6927=PRODUCT('Flat Washer - M6','Flat Washer - M6','Flat Washer - M6',
(#6920));
#7004=COLOUR_RGB('Black',0.12,0.14,0.17);
#7005=FILL_AREA_STYLE_COLOUR('',#7004);
#7006=FILL_AREA_STYLE('',(#7005));
#7007=SURFACE_STYLE_FILL_AREA(#7006);
#7008=SURFACE_SIDE_STYLE('',(#7007));
#7009=SURFACE_STYLE_USAGE(.BOTH.,#7008);
#7010=PRESENTATION_STYLE_ASSIGNMENT((#7009));
ENDSEC;
END-ISO-10303-21;
